ISO-10303-21;
HEADER;
/* Generated by software containing ST-Developer
 * from STEP Tools, Inc. (www.steptools.com) 
 */

FILE_DESCRIPTION(
/* description */ ('Independent hinged machine back cover with retained hinge pins, perim
eter gasket and quarter-turn cam latch. Nominal cover 360 x 260 x 3 mm
, frame 430 x 300 x 20 mm. No guarding, structural or ingress rating a
ssigned.'),
/* implementation_level */ '2;1');

FILE_NAME(
/* name */ 'Latch thrust washer.step',
/* time_stamp */ '2026-11-09T19:36:59-08:00',
/* author */ (''),
/* organization */ (''),
/* preprocessor_version */ 'ST-DEVELOPER v20.2',
/* originating_system */ 'Autodesk Translation Framework v15.17.0.0',
/* authorisation */ '');

FILE_SCHEMA (('AUTOMOTIVE_DESIGN { 1 0 10303 214 3 1 1 }'));
ENDSEC;

DATA;
#10=MECHANICAL_DESIGN_GEOMETRIC_PRESENTATION_REPRESENTATION('',(#203),#32627);
#167=SHAPE_REPRESENTATION_RELATIONSHIP('SRR','None',#32713,#185);
#185=ADVANCED_BREP_SHAPE_REPRESENTATION('',(#221),#32614);
#203=STYLED_ITEM('',(#32812),#221);
#221=MANIFOLD_SOLID_BREP('Body1',#8680);
#260=FACE_BOUND('',#1217,.T.);
#261=FACE_BOUND('',#1219,.T.);
#376=PLANE('',#9203);
#377=PLANE('',#9204);
#713=FACE_OUTER_BOUND('',#1214,.T.);
#714=FACE_OUTER_BOUND('',#1215,.T.);
#715=FACE_OUTER_BOUND('',#1216,.T.);
#716=FACE_OUTER_BOUND('',#1218,.T.);
#1214=EDGE_LOOP('',(#6813,#6814,#6815,#6816));
#1215=EDGE_LOOP('',(#6817,#6818,#6819,#6820));
#1216=EDGE_LOOP('',(#6821));
#1217=EDGE_LOOP('',(#6822));
#1218=EDGE_LOOP('',(#6823));
#1219=EDGE_LOOP('',(#6824));
#1508=CIRCLE('',#9198,4.);
#1509=CIRCLE('',#9199,4.);
#1510=CIRCLE('',#9201,8.);
#1511=CIRCLE('',#9202,8.);
#2476=LINE('',#24270,#3022);
#2477=LINE('',#24276,#3023);
#3022=VECTOR('',#10444,4.);
#3023=VECTOR('',#10451,8.);
#3749=VERTEX_POINT('',#24267);
#3750=VERTEX_POINT('',#24269);
#3751=VERTEX_POINT('',#24273);
#3752=VERTEX_POINT('',#24275);
#4830=EDGE_CURVE('',#3749,#3749,#1508,.T.);
#4831=EDGE_CURVE('',#3749,#3750,#2476,.T.);
#4832=EDGE_CURVE('',#3750,#3750,#1509,.T.);
#4833=EDGE_CURVE('',#3751,#3751,#1510,.T.);
#4834=EDGE_CURVE('',#3751,#3752,#2477,.T.);
#4835=EDGE_CURVE('',#3752,#3752,#1511,.T.);
#6813=ORIENTED_EDGE('',*,*,#4830,.F.);
#6814=ORIENTED_EDGE('',*,*,#4831,.T.);
#6815=ORIENTED_EDGE('',*,*,#4832,.T.);
#6816=ORIENTED_EDGE('',*,*,#4831,.F.);
#6817=ORIENTED_EDGE('',*,*,#4833,.F.);
#6818=ORIENTED_EDGE('',*,*,#4834,.T.);
#6819=ORIENTED_EDGE('',*,*,#4835,.T.);
#6820=ORIENTED_EDGE('',*,*,#4834,.F.);
#6821=ORIENTED_EDGE('',*,*,#4833,.T.);
#6822=ORIENTED_EDGE('',*,*,#4830,.T.);
#6823=ORIENTED_EDGE('',*,*,#4835,.F.);
#6824=ORIENTED_EDGE('',*,*,#4832,.F.);
#8073=CYLINDRICAL_SURFACE('',#9197,4.);
#8074=CYLINDRICAL_SURFACE('',#9200,8.);
#8461=ADVANCED_FACE('',(#713),#8073,.F.);
#8462=ADVANCED_FACE('',(#714),#8074,.T.);
#8463=ADVANCED_FACE('',(#715,#260),#376,.T.);
#8464=ADVANCED_FACE('',(#716,#261),#377,.F.);
#8680=CLOSED_SHELL('',(#8461,#8462,#8463,#8464));
#9196=AXIS2_PLACEMENT_3D('',#24265,#10438,#10439);
#9197=AXIS2_PLACEMENT_3D('',#24266,#10440,#10441);
#9198=AXIS2_PLACEMENT_3D('',#24268,#10442,#10443);
#9199=AXIS2_PLACEMENT_3D('',#24271,#10445,#10446);
#9200=AXIS2_PLACEMENT_3D('',#24272,#10447,#10448);
#9201=AXIS2_PLACEMENT_3D('',#24274,#10449,#10450);
#9202=AXIS2_PLACEMENT_3D('',#24277,#10452,#10453);
#9203=AXIS2_PLACEMENT_3D('',#24278,#10454,#10455);
#9204=AXIS2_PLACEMENT_3D('',#24279,#10456,#10457);
#10438=DIRECTION('axis',(0.,0.,1.));
#10439=DIRECTION('refdir',(1.,0.,0.));
#10440=DIRECTION('center_axis',(0.,0.,1.));
#10441=DIRECTION('ref_axis',(1.,0.,0.));
#10442=DIRECTION('center_axis',(0.,0.,-1.));
#10443=DIRECTION('ref_axis',(1.,0.,0.));
#10444=DIRECTION('',(0.,0.,-1.));
#10445=DIRECTION('center_axis',(0.,0.,-1.));
#10446=DIRECTION('ref_axis',(1.,0.,0.));
#10447=DIRECTION('center_axis',(0.,0.,1.));
#10448=DIRECTION('ref_axis',(1.,0.,0.));
#10449=DIRECTION('center_axis',(0.,0.,1.));
#10450=DIRECTION('ref_axis',(1.,0.,0.));
#10451=DIRECTION('',(0.,0.,-1.));
#10452=DIRECTION('center_axis',(0.,0.,1.));
#10453=DIRECTION('ref_axis',(1.,0.,0.));
#10454=DIRECTION('center_axis',(0.,0.,1.));
#10455=DIRECTION('ref_axis',(1.,0.,0.));
#10456=DIRECTION('center_axis',(0.,0.,1.));
#10457=DIRECTION('ref_axis',(1.,0.,0.));
#24265=CARTESIAN_POINT('',(0.,0.,0.));
#24266=CARTESIAN_POINT('Origin',(0.,0.,0.));
#24267=CARTESIAN_POINT('',(-4.,-4.89858719658941E-16,1.));
#24268=CARTESIAN_POINT('Origin',(0.,0.,1.));
#24269=CARTESIAN_POINT('',(-4.,-4.89858719658941E-16,0.));
#24270=CARTESIAN_POINT('',(-4.,-4.89858719658941E-16,0.));
#24271=CARTESIAN_POINT('Origin',(0.,0.,0.));
#24272=CARTESIAN_POINT('Origin',(0.,0.,0.));
#24273=CARTESIAN_POINT('',(-8.,-9.79717439317883E-16,1.));
#24274=CARTESIAN_POINT('Origin',(0.,0.,1.));
#24275=CARTESIAN_POINT('',(-8.,-9.79717439317883E-16,0.));
#24276=CARTESIAN_POINT('',(-8.,-9.79717439317883E-16,0.));
#24277=CARTESIAN_POINT('Origin',(0.,0.,0.));
#24278=CARTESIAN_POINT('Origin',(0.,0.,1.));
#24279=CARTESIAN_POINT('Origin',(0.,0.,0.));
#32594=UNCERTAINTY_MEASURE_WITH_UNIT(LENGTH_MEASURE(0.01),#32628,
'DISTANCE_ACCURACY_VALUE',
'Maximum model space distance between geometric entities at asserted c
onnectivities');
#32607=UNCERTAINTY_MEASURE_WITH_UNIT(LENGTH_MEASURE(0.01),#32628,
'DISTANCE_ACCURACY_VALUE',
'Maximum model space distance between geometric entities at asserted c
onnectivities');
#32614=(
GEOMETRIC_REPRESENTATION_CONTEXT(3)
GLOBAL_UNCERTAINTY_ASSIGNED_CONTEXT((#32594))
GLOBAL_UNIT_ASSIGNED_CONTEXT((#32628,#32630,#32631))
REPRESENTATION_CONTEXT('','3D')
);
#32627=(
GEOMETRIC_REPRESENTATION_CONTEXT(3)
GLOBAL_UNCERTAINTY_ASSIGNED_CONTEXT((#32607))
GLOBAL_UNIT_ASSIGNED_CONTEXT((#32628,#32630,#32631))
REPRESENTATION_CONTEXT('','3D')
);
#32628=(
LENGTH_UNIT()
NAMED_UNIT(*)
SI_UNIT(.MILLI.,.METRE.)
);
#32630=(
NAMED_UNIT(*)
PLANE_ANGLE_UNIT()
SI_UNIT($,.RADIAN.)
);
#32631=(
NAMED_UNIT(*)
SI_UNIT($,.STERADIAN.)
SOLID_ANGLE_UNIT()
);
#32638=SHAPE_DEFINITION_REPRESENTATION(#32657,#32713);
#32657=PRODUCT_DEFINITION_SHAPE('',$,#32733);
#32713=SHAPE_REPRESENTATION('',(#9196),#32614);
#32726=PRODUCT_DEFINITION_CONTEXT('part definition',#32785,'design');
#32733=PRODUCT_DEFINITION('Latch thrust washer','Latch thrust washer',#32752,
#32726);
#32752=PRODUCT_DEFINITION_FORMATION('',$,#32793);
#32785=APPLICATION_CONTEXT(
'Core Data for Automotive Mechanical Design Process');
#32786=PRODUCT_CONTEXT('part definition',#32785,'mechanical');
#32793=PRODUCT('Latch thrust washer','Latch thrust washer',$,(#32786));
#32812=PRESENTATION_STYLE_ASSIGNMENT((#32819));
#32819=SURFACE_STYLE_USAGE(.BOTH.,#32826);
#32826=SURFACE_SIDE_STYLE('',(#32833));
#32833=SURFACE_STYLE_FILL_AREA(#32840);
#32840=FILL_AREA_STYLE('Light gray',(#32847));
#32847=FILL_AREA_STYLE_COLOUR('Light gray',#32854);
#32854=COLOUR_RGB('Light gray',0.725490196078431,0.752941176470588,0.792156862745098);
ENDSEC;
END-ISO-10303-21;
